ISO-10303-21;
HEADER;
FILE_DESCRIPTION (('STEP AP214'),
    '1' );
FILE_NAME ('Part2.step',
    '2026-10-09T17:48:21',
    ( '' ),
    ( '' ),
    'SwSTEP 2.0',
    'SolidWorks 2024',
    '' );
FILE_SCHEMA (( 'AUTOMOTIVE_DESIGN' ));
ENDSEC;

DATA;
#81=CARTESIAN_POINT ( 'NONE',  ( -46.58670980944423690, 5.000000000000000000, 89.50956111919107627 ) ) ;
#94=VECTOR ( 'NONE', #206, 1000.000000000000114 ) ;
#119=EDGE_CURVE ( 'NONE', #467, #14870, #5816, .T. ) ;
#129=DIRECTION ( 'NONE',  ( 0.000000000000000000, 0.000000000000000000, 1.000000000000000000 ) ) ;
#131=ORIENTED_EDGE ( 'NONE', *, *, #12812, .T. ) ;
#180=VECTOR ( 'NONE', #527, 1000.000000000000000 ) ;
#185=FACE_OUTER_BOUND ( 'NONE', #11001, .T. ) ;
#188=VERTEX_POINT ( 'NONE', #368 ) ;
#199=CARTESIAN_POINT ( 'NONE',  ( 57.41329019055577021, 5.000000000000001776, 97.50956111919106206 ) ) ;
#204=VECTOR ( 'NONE', #14939, 1000.000000000000114 ) ;
#206=DIRECTION ( 'NONE',  ( 0.7071067811865451302, -0.000000000000000000, -0.7071067811865500152 ) ) ;
#211=ORIENTED_EDGE ( 'NONE', *, *, #10659, .T. ) ;
#238=CARTESIAN_POINT ( 'NONE',  ( -44.58670980944422269, 5.000000000000000000, 89.50956111919107627 ) ) ;
#261=FILL_AREA_STYLE_COLOUR ( '', #11287 ) ;
#276=LINE ( 'NONE', #5026, #94 ) ;
#285=AXIS2_PLACEMENT_3D ( 'NONE', #3423, #3496, #1409 ) ;
#289=APPLICATION_CONTEXT ( 'automotive_design' ) ;
#294=ORIENTED_EDGE ( 'NONE', *, *, #12494, .T. ) ;
#301=EDGE_LOOP ( 'NONE', ( #12633, #387, #14477, #1085, #12635, #5840, #11093, #4526 ) ) ;
#338=DIRECTION ( 'NONE',  ( -0.000000000000000000, 1.000000000000000000, -0.000000000000000000 ) ) ;
#368=CARTESIAN_POINT ( 'NONE',  ( -44.58670980944422269, 0.000000000000000000, 89.50956111919107627 ) ) ;
#374=STYLED_ITEM ( 'NONE', ( #8267 ), #385 ) ;
#385=MANIFOLD_SOLID_BREP ( 'Chamfer1', #11506 ) ;
#387=ORIENTED_EDGE ( 'NONE', *, *, #8641, .T. ) ;
#414=FACE_OUTER_BOUND ( 'NONE', #10961, .T. ) ;
#422=CARTESIAN_POINT ( 'NONE',  ( 68.41329019055577021, 0.000000000000000000, 135.5095611191910621 ) ) ;
#441=CARTESIAN_POINT ( 'NONE',  ( 57.41329019055577021, 5.000000000000001776, 125.5408111191910763 ) ) ;
#467=VERTEX_POINT ( 'NONE', #2679 ) ;
#498=DIRECTION ( 'NONE',  ( -0.000000000000000000, 1.000000000000000000, -0.000000000000000000 ) ) ;
#527=DIRECTION ( 'NONE',  ( 8.034405899049458729E-17, 0.7547095802227716810, -0.6560590289905077199 ) ) ;
#529=AXIS2_PLACEMENT_3D ( 'NONE', #13605, #6407, #8706 ) ;
#598=EDGE_CURVE ( 'NONE', #7295, #15255, #3873, .T. ) ;
#658=DIRECTION ( 'NONE',  ( 8.034405899049458729E-17, 0.7547095802227716810, -0.6560590289905077199 ) ) ;
#710=ORIENTED_EDGE ( 'NONE', *, *, #7264, .F. ) ;
#711=ADVANCED_FACE ( 'NONE', ( #14882 ), #12425, .F. ) ;
#723=ORIENTED_EDGE ( 'NONE', *, *, #792, .F. ) ;
#732=DIRECTION ( 'NONE',  ( -0.000000000000000000, 1.000000000000000000, -0.000000000000000000 ) ) ;
#763=CARTESIAN_POINT ( 'NONE',  ( -35.58670980944424400, 5.000000000000000000, 131.2954986191910791 ) ) ;
#765=CARTESIAN_POINT ( 'NONE',  ( 57.41329019055577021, 5.000000000000000000, 95.72362361919107343 ) ) ;
#792=EDGE_CURVE ( 'NONE', #7940, #3694, #4366, .T. ) ;
#794=DIRECTION ( 'NONE',  ( -0.000000000000000000, 1.000000000000000000, -0.000000000000000000 ) ) ;
#831=EDGE_LOOP ( 'NONE', ( #4724, #1877 ) ) ;
#848=DIRECTION ( 'NONE',  ( -0.000000000000000000, 1.000000000000000000, -0.000000000000000000 ) ) ;
#871=AXIS2_PLACEMENT_3D ( 'NONE', #13865, #1924, #4183 ) ;
#904=ADVANCED_FACE ( 'NONE', ( #10542 ), #4128, .F. ) ;
#912=EDGE_CURVE ( 'NONE', #3825, #2695, #14769, .T. ) ;
#1000=CARTESIAN_POINT ( 'NONE',  ( 68.41329019055577021, 5.000000000000000000, 91.50956111919110469 ) ) ;
#1033=( GEOMETRIC_REPRESENTATION_CONTEXT ( 3 ) GLOBAL_UNCERTAINTY_ASSIGNED_CONTEXT ( ( #9938 ) ) GLOBAL_UNIT_ASSIGNED_CONTEXT ( ( #4952, #11854, #14327 ) ) REPRESENTATION_CONTEXT ( 'NONE', 'WORKASPACE' ) );
#1069=DIRECTION ( 'NONE',  ( -0.7071067811865500152, -0.000000000000000000, -0.7071067811865451302 ) ) ;
#1076=LINE ( 'NONE', #9376, #15049 ) ;
#1081=AXIS2_PLACEMENT_3D ( 'NONE', #13581, #5203, #2785 ) ;
#1085=ORIENTED_EDGE ( 'NONE', *, *, #2902, .T. ) ;
#1103=CARTESIAN_POINT ( 'NONE',  ( 57.41329019055577021, 0.000000000000000000, 129.5095611191910621 ) ) ;
#1111=VERTEX_POINT ( 'NONE', #4315 ) ;
#1128=CIRCLE ( 'NONE', #11785, 3.968749999999992895 ) ;
#1138=DIRECTION ( 'NONE',  ( 0.000000000000000000, 1.000000000000000000, 0.000000000000000000 ) ) ;
#1200=DIRECTION ( 'NONE',  ( -0.000000000000000000, 1.000000000000000000, -0.000000000000000000 ) ) ;
#1266=CARTESIAN_POINT ( 'NONE',  ( 57.41329019055577021, 0.000000000000000000, 95.72362361919107343 ) ) ;
#1276=ORIENTED_EDGE ( 'NONE', *, *, #5565, .T. ) ;
#1290=DIRECTION ( 'NONE',  ( 0.000000000000000000, 1.000000000000000000, 0.000000000000000000 ) ) ;
#1292=VECTOR ( 'NONE', #15054, 1000.000000000000000 ) ;
#1325=DIRECTION ( 'NONE',  ( 0.000000000000000000, 1.000000000000000000, 0.000000000000000000 ) ) ;
#1338=ORIENTED_EDGE ( 'NONE', *, *, #14365, .T. ) ;
#1366=EDGE_CURVE ( 'NONE', #12409, #2967, #15008, .T. ) ;
#1371=DIRECTION ( 'NONE',  ( 0.000000000000000000, 0.000000000000000000, 1.000000000000000000 ) ) ;
#1375=VECTOR ( 'NONE', #658, 1000.000000000000000 ) ;
#1393=CARTESIAN_POINT ( 'NONE',  ( -35.58670980944424400, 5.000000000000000000, 129.5095611191910621 ) ) ;
#1409=DIRECTION ( 'NONE',  ( 1.000000000000000000, 0.000000000000000000, 0.000000000000000000 ) ) ;
#1412=CIRCLE ( 'NONE', #10066, 3.968749999999992895 ) ;
#1435=EDGE_CURVE ( 'NONE', #15063, #11245, #4857, .T. ) ;
#1457=CARTESIAN_POINT ( 'NONE',  ( -46.58670980944423690, 5.000000000000000000, 89.50956111919107627 ) ) ;
#1458=SHAPE_REPRESENTATION_RELATIONSHIP ( 'NONE' , 'NONE' ,  #6613, #9048 ) ;
#1463=ORIENTED_EDGE ( 'NONE', *, *, #12940, .F. ) ;
#1465=CARTESIAN_POINT ( 'NONE',  ( 68.41329019055577021, 5.000000000000000000, 135.5095611191910621 ) ) ;
#1470=EDGE_CURVE ( 'NONE', #14932, #2765, #1412, .T. ) ;
#1478=ORIENTED_EDGE ( 'NONE', *, *, #4198, .F. ) ;
#1489=EDGE_CURVE ( 'NONE', #8820, #10769, #12802, .T. ) ;
#1527=ORIENTED_EDGE ( 'NONE', *, *, #15018, .T. ) ;
#1536=AXIS2_PLACEMENT_3D ( 'NONE', #13043, #7148, #11869 ) ;
#1565=DIRECTION ( 'NONE',  ( -0.000000000000000000, 1.000000000000000000, -0.000000000000000000 ) ) ;
#1592=ADVANCED_FACE ( 'NONE', ( #7656 ), #3208, .F. ) ;
#1593=ORIENTED_EDGE ( 'NONE', *, *, #4513, .F. ) ;
#1652=EDGE_LOOP ( 'NONE', ( #11220, #6715, #9351, #2408 ) ) ;
#1661=DIRECTION ( 'NONE',  ( 0.000000000000000000, -1.000000000000000000, 0.000000000000000000 ) ) ;
#1707=LINE ( 'NONE', #11168, #13498 ) ;
#1716=CARTESIAN_POINT ( 'NONE',  ( 57.41329019055577021, 2.488961461112888074, 129.5095611191910621 ) ) ;
#1773=VECTOR ( 'NONE', #14677, 1000.000000000000000 ) ;
#1784=LINE ( 'NONE', #4043, #7266 ) ;
#1836=AXIS2_PLACEMENT_3D ( 'NONE', #14259, #1069, #12023 ) ;
#1837=AXIS2_PLACEMENT_3D ( 'NONE', #11615, #4553, #10513 ) ;
#1866=PLANE ( 'NONE',  #13318 ) ;
#1877=ORIENTED_EDGE ( 'NONE', *, *, #6236, .F. ) ;
#1889=AXIS2_PLACEMENT_3D ( 'NONE', #8733, #7514, #3860 ) ;
#1896=AXIS2_PLACEMENT_3D ( 'NONE', #9000, #1565, #11335 ) ;
#1924=DIRECTION ( 'NONE',  ( 0.000000000000000000, 1.000000000000000000, 0.000000000000000000 ) ) ;
#1968=VERTEX_POINT ( 'NONE', #14747 ) ;
#2006=LINE ( 'NONE', #4264, #13282 ) ;
#2087=CARTESIAN_POINT ( 'NONE',  ( -46.58670980944423690, 0.000000000000000000, 89.50956111919107627 ) ) ;
#2089=VECTOR ( 'NONE', #3773, 1000.000000000000000 ) ;
#2132=DIRECTION ( 'NONE',  ( 0.000000000000000000, 0.000000000000000000, 1.000000000000000000 ) ) ;
#2142=ORIENTED_EDGE ( 'NONE', *, *, #7330, .F. ) ;
#2148=VECTOR ( 'NONE', #848, 1000.000000000000000 ) ;
#2151=DIRECTION ( 'NONE',  ( 0.000000000000000000, 1.000000000000000000, 0.000000000000000000 ) ) ;
#2195=ORIENTED_EDGE ( 'NONE', *, *, #4021, .T. ) ;
#2211=ORIENTED_EDGE ( 'NONE', *, *, #2902, .F. ) ;
#2225=EDGE_LOOP ( 'NONE', ( #13748, #10679 ) ) ;
#2235=DIRECTION ( 'NONE',  ( 0.7071067811865525687, -0.000000000000000000, -0.7071067811865425767 ) ) ;
#2247=CYLINDRICAL_SURFACE ( 'NONE', #4789, 1.785937500000001066 ) ;
#2248=ORIENTED_EDGE ( 'NONE', *, *, #8490, .F. ) ;
#2266=ORIENTED_EDGE ( 'NONE', *, *, #14266, .T. ) ;
#2270=VECTOR ( 'NONE', #9483, 1000.000000000000000 ) ;
#2278=ADVANCED_FACE ( 'NONE', ( #5760 ), #2247, .F. ) ;
#2285=SHAPE_DEFINITION_REPRESENTATION ( #13060, #6613 ) ;
#2289=ORIENTED_EDGE ( 'NONE', *, *, #13237, .F. ) ;
#2294=VECTOR ( 'NONE', #13514, 1000.000000000000000 ) ;
#2317=CARTESIAN_POINT ( 'NONE',  ( 66.41329019055577021, 0.000000000000000000, 89.50956111919107627 ) ) ;
#2396=CYLINDRICAL_SURFACE ( 'NONE', #3642, 1.785937500000001066 ) ;
#2401=CARTESIAN_POINT ( 'NONE',  ( -46.58670980944423690, 0.000000000000000000, 89.50956111919107627 ) ) ;
#2408=ORIENTED_EDGE ( 'NONE', *, *, #598, .T. ) ;
#2424=DIRECTION ( 'NONE',  ( 0.000000000000000000, -1.000000000000000000, 0.000000000000000000 ) ) ;
#2437=DIRECTION ( 'NONE',  ( -0.000000000000000000, 1.000000000000000000, -0.000000000000000000 ) ) ;
#2451=DIRECTION ( 'NONE',  ( 0.000000000000000000, 0.000000000000000000, 1.000000000000000000 ) ) ;
#2478=ORIENTED_EDGE ( 'NONE', *, *, #1366, .F. ) ;
#2483=EDGE_CURVE ( 'NONE', #2967, #12409, #9991, .T. ) ;
#2490=DIRECTION ( 'NONE',  ( 0.000000000000000000, 0.000000000000000000, 1.000000000000000000 ) ) ;
#2503=CONICAL_SURFACE ( 'NONE', #12164, 3.968749999999992895, 0.7155849933176756661 ) ;
#2507=AXIS2_PLACEMENT_3D ( 'NONE', #7567, #10094, #3977 ) ;
#2511=DIRECTION ( 'NONE',  ( -0.000000000000000000, 1.000000000000000000, -0.000000000000000000 ) ) ;
#2545=CARTESIAN_POINT ( 'NONE',  ( -44.58670980944423690, 5.000000000000000000, 137.5095611191910621 ) ) ;
#2578=CARTESIAN_POINT ( 'NONE',  ( -35.58670980944424400, 0.000000000000000000, 131.2954986191910791 ) ) ;
#2590=CONICAL_SURFACE ( 'NONE', #4333, 3.968749999999992895, 0.7155849933176756661 ) ;
#2609=CARTESIAN_POINT ( 'NONE',  ( 0.000000000000000000, 5.000000000000000000, 0.000000000000000000 ) ) ;
#2650=DIRECTION ( 'NONE',  ( 0.000000000000000000, -0.000000000000000000, 1.000000000000000000 ) ) ;
#2665=AXIS2_PLACEMENT_3D ( 'NONE', #12777, #11378, #10059 ) ;
#2676=CARTESIAN_POINT ( 'NONE',  ( -44.58670980944423690, 5.000000000000000000, 137.5095611191910621 ) ) ;
#2679=CARTESIAN_POINT ( 'NONE',  ( -35.58670980944424400, 0.000000000000000000, 127.7236236191910734 ) ) ;
#2688=DIRECTION ( 'NONE',  ( 0.000000000000000000, 0.000000000000000000, 1.000000000000000000 ) ) ;
#2690=FACE_BOUND ( 'NONE', #2225, .T. ) ;
#2695=VERTEX_POINT ( 'NONE', #12866 ) ;
#2765=VERTEX_POINT ( 'NONE', #14023 ) ;
#2785=DIRECTION ( 'NONE',  ( 0.000000000000000000, 0.000000000000000000, 1.000000000000000000 ) ) ;
#2825=DIRECTION ( 'NONE',  ( -1.000000000000000000, 0.000000000000000000, -0.000000000000000000 ) ) ;
#2827=EDGE_LOOP ( 'NONE', ( #2211, #4842, #5535, #10590 ) ) ;
#2844=DIRECTION ( 'NONE',  ( -0.000000000000000000, 1.000000000000000000, -0.000000000000000000 ) ) ;
#2870=EDGE_LOOP ( 'NONE', ( #14382, #8170, #1463, #2266, #1478, #6999, #9026, #15219 ) ) ;
#2893=ADVANCED_FACE ( 'NONE', ( #7207 ), #10916, .F. ) ;
#2895=ORIENTED_EDGE ( 'NONE', *, *, #9965, .F. ) ;
#2902=EDGE_CURVE ( 'NONE', #6954, #14499, #276, .T. ) ;
#2905=DIRECTION ( 'NONE',  ( 0.000000000000000000, 0.000000000000000000, 1.000000000000000000 ) ) ;
#2957=CARTESIAN_POINT ( 'NONE',  ( 66.41329019055578442, 5.000000000000000000, 137.5095611191910621 ) ) ;
#2967=VERTEX_POINT ( 'NONE', #9836 ) ;
#2978=CARTESIAN_POINT ( 'NONE',  ( 68.41329019055577021, 0.000000000000000000, 135.5095611191910621 ) ) ;
#3002=ORIENTED_EDGE ( 'NONE', *, *, #6236, .T. ) ;
#3025=VECTOR ( 'NONE', #12618, 1000.000000000000000 ) ;
#3029=CARTESIAN_POINT ( 'NONE',  ( -35.58670980944424400, 5.000000000000001776, 93.54081111919107627 ) ) ;
#3036=CARTESIAN_POINT ( 'NONE',  ( -44.58670980944423690, 0.000000000000000000, 137.5095611191910621 ) ) ;
#3089=CARTESIAN_POINT ( 'NONE',  ( -35.58670980944424400, 5.000000000000001776, 101.4783111191910621 ) ) ;
#3126=AXIS2_PLACEMENT_3D ( 'NONE', #4051, #11261, #14742 ) ;
#3164=CARTESIAN_POINT ( 'NONE',  ( -46.58670980944423690, 5.000000000000000000, 135.5095611191910621 ) ) ;
#3208=CYLINDRICAL_SURFACE ( 'NONE', #6647, 1.785937500000001066 ) ;
#3216=DIRECTION ( 'NONE',  ( -0.7071067811865425767, 0.000000000000000000, -0.7071067811865525687 ) ) ;
#3229=DIRECTION ( 'NONE',  ( 0.000000000000000000, 0.000000000000000000, 1.000000000000000000 ) ) ;
#3230=CARTESIAN_POINT ( 'NONE',  ( 57.41329019055577021, 5.000000000000000000, 129.5095611191910621 ) ) ;
#3231=DIRECTION ( 'NONE',  ( 0.000000000000000000, 1.000000000000000000, 0.000000000000000000 ) ) ;
#3262=ADVANCED_FACE ( 'NONE', ( #14241 ), #7960, .F. ) ;
#3333=DIRECTION ( 'NONE',  ( 0.000000000000000000, 1.000000000000000000, 0.000000000000000000 ) ) ;
#3340=ORIENTED_EDGE ( 'NONE', *, *, #11042, .T. ) ;
#3357=ORIENTED_EDGE ( 'NONE', *, *, #14266, .F. ) ;
#3360=EDGE_LOOP ( 'NONE', ( #12573, #15118, #5472, #6061 ) ) ;
#3399=VERTEX_POINT ( 'NONE', #9736 ) ;
#3401=VERTEX_POINT ( 'NONE', #11922 ) ;
#3414=LINE ( 'NONE', #6991, #14452 ) ;
#3419=ORIENTED_EDGE ( 'NONE', *, *, #9949, .T. ) ;
#3423=CARTESIAN_POINT ( 'NONE',  ( 0.000000000000000000, 0.000000000000000000, 0.000000000000000000 ) ) ;
#3425=EDGE_CURVE ( 'NONE', #9134, #15255, #12151, .T. ) ;
#3426=DIRECTION ( 'NONE',  ( -0.000000000000000000, 1.000000000000000000, -0.000000000000000000 ) ) ;
#3496=DIRECTION ( 'NONE',  ( 0.000000000000000000, 0.000000000000000000, 1.000000000000000000 ) ) ;
#3498=FACE_OUTER_BOUND ( 'NONE', #10090, .T. ) ;
#3503=CARTESIAN_POINT ( 'NONE',  ( 26.34657265215283317, 5.000000000000000000, 89.50956111919107627 ) ) ;
#3522=ADVANCED_FACE ( 'NONE', ( #7356 ), #2590, .F. ) ;
#3527=ADVANCED_FACE ( 'NONE', ( #8358 ), #11271, .F. ) ;
#3552=ORIENTED_EDGE ( 'NONE', *, *, #9609, .F. ) ;
#3558=FACE_OUTER_BOUND ( 'NONE', #2827, .T. ) ;
#3588=DIRECTION ( 'NONE',  ( -0.000000000000000000, 1.000000000000000000, -0.000000000000000000 ) ) ;
#3642=AXIS2_PLACEMENT_3D ( 'NONE', #1393, #8293, #7066 ) ;
#3655=EDGE_LOOP ( 'NONE', ( #8071, #2478, #9762, #13732 ) ) ;
#3656=ORIENTED_EDGE ( 'NONE', *, *, #8641, .F. ) ;
#3662=CARTESIAN_POINT ( 'NONE',  ( 57.41329019055577021, 0.000000000000000000, 99.29549861919106490 ) ) ;
#3690=ORIENTED_EDGE ( 'NONE', *, *, #12494, .F. ) ;
#3694=VERTEX_POINT ( 'NONE', #5548 ) ;
#3697=DIRECTION ( 'NONE',  ( -0.000000000000000000, 1.000000000000000000, -0.000000000000000000 ) ) ;
#3699=FACE_BOUND ( 'NONE', #831, .T. ) ;
#3755=VECTOR ( 'NONE', #5636, 1000.000000000000000 ) ;
#3756=LINE ( 'NONE', #13230, #11003 ) ;
#3763=EDGE_CURVE ( 'NONE', #14989, #3401, #14972, .T. ) ;
#3765=SURFACE_STYLE_USAGE ( .BOTH. , #8573 ) ;
#3773=DIRECTION ( 'NONE',  ( 8.034405899049458729E-17, 0.7547095802227716810, -0.6560590289905077199 ) ) ;
#3779=ORIENTED_EDGE ( 'NONE', *, *, #14086, .T. ) ;
#3793=CARTESIAN_POINT ( 'NONE',  ( -44.58670980944423690, 0.000000000000000000, 137.5095611191910621 ) ) ;
#3825=VERTEX_POINT ( 'NONE', #9468 ) ;
#3860=DIRECTION ( 'NONE',  ( 0.000000000000000000, 0.000000000000000000, 1.000000000000000000 ) ) ;
#3873=CIRCLE ( 'NONE', #5613, 3.968749999999992895 ) ;
#3892=FACE_BOUND ( 'NONE', #13411, .T. ) ;
#3905=EDGE_CURVE ( 'NONE', #9134, #7307, #7819, .T. ) ;
#3977=DIRECTION ( 'NONE',  ( 0.000000000000000000, 0.000000000000000000, 1.000000000000000000 ) ) ;
#4007=CIRCLE ( 'NONE', #2507, 3.968749999999992895 ) ;
#4010=EDGE_LOOP ( 'NONE', ( #5759, #11391, #7857, #3340 ) ) ;
#4021=EDGE_CURVE ( 'NONE', #14870, #467, #9284, .T. ) ;
#4026=CIRCLE ( 'NONE', #7983, 1.785937500000001066 ) ;
#4043=CARTESIAN_POINT ( 'NONE',  ( -35.58670980944424400, 5.000000000000000000, 127.7236236191910734 ) ) ;
#4051=CARTESIAN_POINT ( 'NONE',  ( -35.58670980944424400, 0.000000000000000000, 97.50956111919106206 ) ) ;
#4060=PRODUCT_DEFINITION_CONTEXT ( 'detailed design', #4867, 'design' ) ;
#4128=CONICAL_SURFACE ( 'NONE', #8824, 3.968749999999992895, 0.7155849933176756661 ) ;
#4183=DIRECTION ( 'NONE',  ( 0.000000000000000000, 0.000000000000000000, 1.000000000000000000 ) ) ;
#4197=LINE ( 'NONE', #763, #13212 ) ;
#4198=EDGE_CURVE ( 'NONE', #12948, #188, #14339, .T. ) ;
#4221=EDGE_CURVE ( 'NONE', #6290, #1968, #9301, .T. ) ;
#4250=CARTESIAN_POINT ( 'NONE',  ( 57.41329019055577021, 5.000000000000001776, 129.5095611191910621 ) ) ;
#4253=EDGE_LOOP ( 'NONE', ( #4484, #13637, #15096, #13890 ) ) ;
#4264=CARTESIAN_POINT ( 'NONE',  ( 63.41329019055576310, 0.000000000000000000, 137.5095611191910621 ) ) ;
#4315=CARTESIAN_POINT ( 'NONE',  ( -46.58670980944423690, 0.000000000000000000, 91.50956111919106206 ) ) ;
#4333=AXIS2_PLACEMENT_3D ( 'NONE', #14319, #3697, #2688 ) ;
#4338=EDGE_CURVE ( 'NONE', #12409, #14932, #12333, .T. ) ;
#4366=CIRCLE ( 'NONE', #3126, 1.785937500000001066 ) ;
#4377=ORIENTED_EDGE ( 'NONE', *, *, #9140, .F. ) ;
#4421=CONICAL_SURFACE ( 'NONE', #15059, 3.968749999999992895, 0.7155849933176756661 ) ;
#4472=EDGE_CURVE ( 'NONE', #5280, #6026, #9055, .T. ) ;
#4473=CARTESIAN_POINT ( 'NONE',  ( 57.41329019055577021, 2.488961461112888074, 131.2954986191910791 ) ) ;
#4484=ORIENTED_EDGE ( 'NONE', *, *, #12812, .F. ) ;
#4506=VERTEX_POINT ( 'NONE', #3089 ) ;
#4513=EDGE_CURVE ( 'NONE', #8072, #6629, #10206, .T. ) ;
#4521=LINE ( 'NONE', #3503, #10742 ) ;
#4526=ORIENTED_EDGE ( 'NONE', *, *, #8285, .T. ) ;
#4549=CIRCLE ( 'NONE', #12992, 1.785937500000001066 ) ;
#4553=DIRECTION ( 'NONE',  ( 0.7071067811865425767, 0.000000000000000000, 0.7071067811865525687 ) ) ;
#4567=ORIENTED_EDGE ( 'NONE', *, *, #8285, .F. ) ;
#4582=DIRECTION ( 'NONE',  ( -0.000000000000000000, 1.000000000000000000, -0.000000000000000000 ) ) ;
#4599=EDGE_CURVE ( 'NONE', #3694, #7940, #11053, .T. ) ;
#4624=AXIS2_PLACEMENT_3D ( 'NONE', #11403, #5528, #10229 ) ;
#4641=FACE_OUTER_BOUND ( 'NONE', #15134, .T. ) ;
#4657=CARTESIAN_POINT ( 'NONE',  ( 66.41329019055577021, 5.000000000000000000, 89.50956111919107627 ) ) ;
#4684=CARTESIAN_POINT ( 'NONE',  ( -46.58670980944423690, 5.000000000000000000, 91.50956111919106206 ) ) ;
#4724=ORIENTED_EDGE ( 'NONE', *, *, #13810, .F. ) ;
#4748=VECTOR ( 'NONE', #1661, 1000.000000000000000 ) ;
#4753=LINE ( 'NONE', #4684, #11725 ) ;
#4768=LINE ( 'NONE', #9562, #2270 ) ;
#4789=AXIS2_PLACEMENT_3D ( 'NONE', #15194, #4582, #9307 ) ;
#4808=CIRCLE ( 'NONE', #6066, 3.968749999999992895 ) ;
#4814=DIRECTION ( 'NONE',  ( -1.000000000000000000, -0.000000000000000000, -0.000000000000000000 ) ) ;
#4817=ADVANCED_FACE ( 'NONE', ( #6206 ), #9584, .F. ) ;
#4837=DIRECTION ( 'NONE',  ( -0.000000000000000000, 1.000000000000000000, -0.000000000000000000 ) ) ;
#4842=ORIENTED_EDGE ( 'NONE', *, *, #12745, .F. ) ;
#4855=CARTESIAN_POINT ( 'NONE',  ( -35.58670980944424400, 5.000000000000001776, 129.5095611191910621 ) ) ;
#4857=LINE ( 'NONE', #2676, #5892 ) ;
#4863=( LENGTH_UNIT ( ) NAMED_UNIT ( * ) SI_UNIT ( .MILLI., .METRE. ) );
#4867=APPLICATION_CONTEXT ( 'automotive_design' ) ;
#4869=ADVANCED_FACE ( 'NONE', ( #12007 ), #5107, .F. ) ;
#4889=EDGE_LOOP ( 'NONE', ( #2195, #14770 ) ) ;
#4913=FACE_OUTER_BOUND ( 'NONE', #2870, .T. ) ;
#4935=DIRECTION ( 'NONE',  ( 0.000000000000000000, 0.000000000000000000, 1.000000000000000000 ) ) ;
#4946=FACE_BOUND ( 'NONE', #6870, .T. ) ;
#4952=( LENGTH_UNIT ( ) NAMED_UNIT ( * ) SI_UNIT ( .MILLI., .METRE. ) );
#4966=CARTESIAN_POINT ( 'NONE',  ( -35.58670980944424400, 5.000000000000001776, 133.4783111191910621 ) ) ;
#5004=FACE_OUTER_BOUND ( 'NONE', #3655, .T. ) ;
#5018=VECTOR ( 'NONE', #3426, 1000.000000000000000 ) ;
#5026=CARTESIAN_POINT ( 'NONE',  ( 101.9614256548736364, 5.000000000000000000, 101.9614256548729259 ) ) ;
#5051=EDGE_LOOP ( 'NONE', ( #4567, #11642, #3357, #15217 ) ) ;
#5056=AXIS2_PLACEMENT_3D ( 'NONE', #9947, #13462, #14530 ) ;
#5057=FACE_BOUND ( 'NONE', #6797, .T. ) ;
#5072=AXIS2_PLACEMENT_3D ( 'NONE', #9662, #8513, #12093 ) ;
#5107=CYLINDRICAL_SURFACE ( 'NONE', #5123, 1.785937500000001066 ) ;
#5123=AXIS2_PLACEMENT_3D ( 'NONE', #13332, #2844, #1371 ) ;
#5159=CARTESIAN_POINT ( 'NONE',  ( -44.58670980944423690, 5.000000000000000000, 137.5095611191910621 ) ) ;
#5203=DIRECTION ( 'NONE',  ( -0.000000000000000000, 1.000000000000000000, -0.000000000000000000 ) ) ;
#5225=CARTESIAN_POINT ( 'NONE',  ( 57.41329019055577021, 0.000000000000000000, 127.7236236191910734 ) ) ;
#5232=AXIS2_PLACEMENT_3D ( 'NONE', #12856, #13099, #9274 ) ;
#5244=LINE ( 'NONE', #8580, #1375 ) ;
#5271=CARTESIAN_POINT ( 'NONE',  ( -35.58670980944424400, 2.488961461112888074, 97.50956111919106206 ) ) ;
#5280=VERTEX_POINT ( 'NONE', #3662 ) ;
#5283=ORIENTED_EDGE ( 'NONE', *, *, #4338, .F. ) ;
#5384=ORIENTED_EDGE ( 'NONE', *, *, #13550, .T. ) ;
#5398=CARTESIAN_POINT ( 'NONE',  ( -46.58670980944423690, 5.000000000000000000, 91.50956111919106206 ) ) ;
#5447=DIRECTION ( 'NONE',  ( -0.000000000000000000, 1.000000000000000000, -0.000000000000000000 ) ) ;
#5472=ORIENTED_EDGE ( 'NONE', *, *, #9965, .T. ) ;
#5482=ORIENTED_EDGE ( 'NONE', *, *, #10184, .F. ) ;
#5497=ORIENTED_EDGE ( 'NONE', *, *, #10659, .F. ) ;
#5503=LINE ( 'NONE', #10204, #204 ) ;
#5521=LINE ( 'NONE', #2957, #2294 ) ;
#5528=DIRECTION ( 'NONE',  ( -0.000000000000000000, 1.000000000000000000, -0.000000000000000000 ) ) ;
#5535=ORIENTED_EDGE ( 'NONE', *, *, #6246, .F. ) ;
#5548=CARTESIAN_POINT ( 'NONE',  ( -35.58670980944424400, 0.000000000000000000, 99.29549861919106490 ) ) ;
#5565=EDGE_CURVE ( 'NONE', #11245, #8515, #2006, .T. ) ;
#5566=DIRECTION ( 'NONE',  ( -0.000000000000000000, 1.000000000000000000, -0.000000000000000000 ) ) ;
#5613=AXIS2_PLACEMENT_3D ( 'NONE', #10806, #4837, #5939 ) ;
#5636=DIRECTION ( 'NONE',  ( 0.000000000000000000, 0.000000000000000000, -1.000000000000000000 ) ) ;
#5664=CYLINDRICAL_SURFACE ( 'NONE', #7259, 1.785937500000001066 ) ;
#5753=EDGE_CURVE ( 'NONE', #8984, #12668, #5244, .T. ) ;
#5759=ORIENTED_EDGE ( 'NONE', *, *, #12940, .T. ) ;
#5760=FACE_OUTER_BOUND ( 'NONE', #12056, .T. ) ;
#5812=DIRECTION ( 'NONE',  ( 0.000000000000000000, 0.000000000000000000, 1.000000000000000000 ) ) ;
#5816=CIRCLE ( 'NONE', #5072, 1.785937500000001066 ) ;
#5832=LINE ( 'NONE', #3793, #10346 ) ;
#5840=ORIENTED_EDGE ( 'NONE', *, *, #13237, .T. ) ;
#5885=DIRECTION ( 'NONE',  ( 0.000000000000000000, 0.000000000000000000, 1.000000000000000000 ) ) ;
#5892=VECTOR ( 'NONE', #6344, 1000.000000000000000 ) ;
#5936=CARTESIAN_POINT ( 'NONE',  ( -35.58670980944424400, 0.000000000000000000, 95.72362361919107343 ) ) ;
#5939=DIRECTION ( 'NONE',  ( 0.000000000000000000, 0.000000000000000000, 1.000000000000000000 ) ) ;
#6007=FACE_BOUND ( 'NONE', #12987, .T. ) ;
#6009=CONICAL_SURFACE ( 'NONE', #7958, 3.968749999999992895, 0.7155849933176756661 ) ;
#6012=DIRECTION ( 'NONE',  ( 0.000000000000000000, 1.000000000000000000, 0.000000000000000000 ) ) ;
#6026=VERTEX_POINT ( 'NONE', #1266 ) ;
#6057=ORIENTED_EDGE ( 'NONE', *, *, #12120, .T. ) ;
#6061=ORIENTED_EDGE ( 'NONE', *, *, #912, .T. ) ;
#6065=PLANE ( 'NONE',  #1836 ) ;
#6066=AXIS2_PLACEMENT_3D ( 'NONE', #11754, #1200, #8109 ) ;
#6090=LINE ( 'NONE', #81, #11801 ) ;
#6112=VECTOR ( 'NONE', #14408, 1000.000000000000000 ) ;
#6166=EDGE_LOOP ( 'NONE', ( #2248, #6307, #3002, #13788 ) ) ;
#6193=DIRECTION ( 'NONE',  ( 0.000000000000000000, 0.000000000000000000, 1.000000000000000000 ) ) ;
#6206=FACE_OUTER_BOUND ( 'NONE', #14515, .T. ) ;
#6236=EDGE_CURVE ( 'NONE', #12668, #4506, #1128, .T. ) ;
#6246=EDGE_CURVE ( 'NONE', #6301, #8515, #13610, .T. ) ;
#6258=CARTESIAN_POINT ( 'NONE',  ( 57.41329019055577021, 5.000000000000001776, 129.5095611191910621 ) ) ;
#6264=ORIENTED_EDGE ( 'NONE', *, *, #13764, .F. ) ;
#6290=VERTEX_POINT ( 'NONE', #12371 ) ;
#6301=VERTEX_POINT ( 'NONE', #422 ) ;
#6307=ORIENTED_EDGE ( 'NONE', *, *, #5753, .T. ) ;
#6314=PLANE ( 'NONE',  #12455 ) ;
#6325=EDGE_CURVE ( 'NONE', #15063, #6954, #12598, .T. ) ;
#6330=VECTOR ( 'NONE', #2235, 999.9999999999998863 ) ;
#6331=AXIS2_PLACEMENT_3D ( 'NONE', #199, #9888, #2451 ) ;
#6344=DIRECTION ( 'NONE',  ( 0.000000000000000000, -1.000000000000000000, 0.000000000000000000 ) ) ;
#6347=ORIENTED_EDGE ( 'NONE', *, *, #13550, .F. ) ;
#6351=EDGE_LOOP ( 'NONE', ( #10902, #9877, #6264, #3419 ) ) ;
#6393=CARTESIAN_POINT ( 'NONE',  ( -46.58670980944423690, 5.000000000000000000, 135.5095611191910621 ) ) ;
#6407=DIRECTION ( 'NONE',  ( -0.000000000000000000, 1.000000000000000000, -0.000000000000000000 ) ) ;
#6449=LINE ( 'NONE', #9987, #12749 ) ;
#6453=PRODUCT_DEFINITION_FORMATION_WITH_SPECIFIED_SOURCE ( 'ANY', '', #9435, .NOT_KNOWN. ) ;
#6454=EDGE_LOOP ( 'NONE', ( #710, #10372, #294, #11874 ) ) ;
#6481=CARTESIAN_POINT ( 'NONE',  ( 57.41329019055577021, 0.000000000000000000, 129.5095611191910621 ) ) ;
#6506=EDGE_CURVE ( 'NONE', #9953, #6629, #6090, .T. ) ;
#6523=ORIENTED_EDGE ( 'NONE', *, *, #792, .T. ) ;
#6613=SHAPE_REPRESENTATION ( 'Part2', ( #285 ), #1033 ) ;
#6629=VERTEX_POINT ( 'NONE', #6393 ) ;
#6647=AXIS2_PLACEMENT_3D ( 'NONE', #13763, #794, #8946 ) ;
#6650=CIRCLE ( 'NONE', #2665, 1.785937500000001066 ) ;
#6652=ORIENTED_EDGE ( 'NONE', *, *, #8404, .F. ) ;
#6694=DIRECTION ( 'NONE',  ( 0.000000000000000000, 0.000000000000000000, 1.000000000000000000 ) ) ;
#6715=ORIENTED_EDGE ( 'NONE', *, *, #8593, .F. ) ;
#6758=LINE ( 'NONE', #2087, #8250 ) ;
#6771=ORIENTED_EDGE ( 'NONE', *, *, #8490, .T. ) ;
#6797=EDGE_LOOP ( 'NONE', ( #12516, #6523 ) ) ;
#6802=LINE ( 'NONE', #10265, #12226 ) ;
#6807=ADVANCED_FACE ( 'NONE', ( #6839 ), #1866, .F. ) ;
#6839=FACE_OUTER_BOUND ( 'NONE', #10740, .T. ) ;
#6861=CARTESIAN_POINT ( 'NONE',  ( -35.58670980944424400, 5.000000000000001776, 97.50956111919106206 ) ) ;
#6863=ORIENTED_EDGE ( 'NONE', *, *, #10184, .T. ) ;
#6869=EDGE_CURVE ( 'NONE', #6026, #2695, #13660, .T. ) ;
#6870=EDGE_LOOP ( 'NONE', ( #7104, #4377 ) ) ;
#6875=CARTESIAN_POINT ( 'NONE',  ( -11.54813546431719473, 5.000000000000000000, 11.54813546431703308 ) ) ;
#6896=DIRECTION ( 'NONE',  ( 0.000000000000000000, 0.000000000000000000, 1.000000000000000000 ) ) ;
#6908=ORIENTED_EDGE ( 'NONE', *, *, #4221, .F. ) ;
#6954=VERTEX_POINT ( 'NONE', #15263 ) ;
#6991=CARTESIAN_POINT ( 'NONE',  ( 68.41329019055577021, 0.000000000000000000, 137.5095611191910621 ) ) ;
#6999=ORIENTED_EDGE ( 'NONE', *, *, #12106, .T. ) ;
#7030=AXIS2_PLACEMENT_3D ( 'NONE', #14996, #5566, #2132 ) ;
#7034=EDGE_LOOP ( 'NONE', ( #8842, #8843, #14985, #12159 ) ) ;
#7048=CARTESIAN_POINT ( 'NONE',  ( 57.41329019055577021, 0.000000000000000000, 97.50956111919106206 ) ) ;
#7066=DIRECTION ( 'NONE',  ( 0.000000000000000000, 0.000000000000000000, 1.000000000000000000 ) ) ;
#7086=ADVANCED_FACE ( 'NONE', ( #11938 ), #2396, .F. ) ;
#7104=ORIENTED_EDGE ( 'NONE', *, *, #598, .F. ) ;
#7129=FACE_BOUND ( 'NONE', #7833, .T. ) ;
#7148=DIRECTION ( 'NONE',  ( -0.000000000000000000, 1.000000000000000000, -0.000000000000000000 ) ) ;
#7204=FACE_OUTER_BOUND ( 'NONE', #301, .T. ) ;
#7207=FACE_OUTER_BOUND ( 'NONE', #6351, .T. ) ;
#7233=PLANE ( 'NONE',  #10188 ) ;
#7259=AXIS2_PLACEMENT_3D ( 'NONE', #3230, #11462, #12782 ) ;
#7264=EDGE_CURVE ( 'NONE', #2695, #8820, #8828, .T. ) ;
#7266=VECTOR ( 'NONE', #5447, 1000.000000000000000 ) ;
#7267=PRODUCT_CONTEXT ( 'NONE', #289, 'mechanical' ) ;
#7295=VERTEX_POINT ( 'NONE', #14936 ) ;
#7307=VERTEX_POINT ( 'NONE', #4473 ) ;
#7330=EDGE_CURVE ( 'NONE', #2695, #3825, #6650, .T. ) ;
#7337=PLANE ( 'NONE',  #12978 ) ;
#7356=FACE_OUTER_BOUND ( 'NONE', #6454, .T. ) ;
#7514=DIRECTION ( 'NONE',  ( -0.000000000000000000, 1.000000000000000000, -0.000000000000000000 ) ) ;
#7567=CARTESIAN_POINT ( 'NONE',  ( -35.58670980944424400, 5.000000000000001776, 129.5095611191910621 ) ) ;
#7571=LINE ( 'NONE', #9943, #4748 ) ;
#7594=CARTESIAN_POINT ( 'NONE',  ( 66.41329019055577021, 0.000000000000000000, 89.50956111919107627 ) ) ;
#7597=ORIENTED_EDGE ( 'NONE', *, *, #13677, .F. ) ;
#7646=CARTESIAN_POINT ( 'NONE',  ( 57.41329019055577021, 5.000000000000000000, 99.29549861919106490 ) ) ;
#7650=CARTESIAN_POINT ( 'NONE',  ( 63.41329019055576310, 5.000000000000000000, 137.5095611191910621 ) ) ;
#7656=FACE_OUTER_BOUND ( 'NONE', #11572, .T. ) ;
#7663=CIRCLE ( 'NONE', #9372, 1.785937500000001066 ) ;
#7708=ORIENTED_EDGE ( 'NONE', *, *, #9609, .T. ) ;
#7715=DIRECTION ( 'NONE',  ( 1.000000000000000000, 0.000000000000000000, 0.000000000000000000 ) ) ;
#7730=FACE_OUTER_BOUND ( 'NONE', #6166, .T. ) ;
#7798=AXIS2_PLACEMENT_3D ( 'NONE', #2545, #9668, #9371 ) ;
#7819=CIRCLE ( 'NONE', #12763, 1.785937500000001066 ) ;
#7833=EDGE_LOOP ( 'NONE', ( #11775, #14818 ) ) ;
#7843=DIRECTION ( 'NONE',  ( 1.000000000000000000, 0.000000000000000000, 0.000000000000000000 ) ) ;
#7847=DIRECTION ( 'NONE',  ( 0.000000000000000000, 0.000000000000000000, 1.000000000000000000 ) ) ;
#7852=DIRECTION ( 'NONE',  ( -0.000000000000000000, 1.000000000000000000, -0.000000000000000000 ) ) ;
#7857=ORIENTED_EDGE ( 'NONE', *, *, #6506, .F. ) ;
#7904=ORIENTED_EDGE ( 'NONE', *, *, #12718, .F. ) ;
#7936=VERTEX_POINT ( 'NONE', #238 ) ;
#7939=CARTESIAN_POINT ( 'NONE',  ( 68.41329019055577021, 5.000000000000000000, 137.5095611191910621 ) ) ;
#7940=VERTEX_POINT ( 'NONE', #5936 ) ;
#7958=AXIS2_PLACEMENT_3D ( 'NONE', #6258, #2437, #11902 ) ;
#7960=PLANE ( 'NONE',  #1837 ) ;
#7983=AXIS2_PLACEMENT_3D ( 'NONE', #7048, #1138, #8042 ) ;
#7995=CARTESIAN_POINT ( 'NONE',  ( 57.41329019055577021, 5.000000000000001776, 125.5408111191910763 ) ) ;
#8042=DIRECTION ( 'NONE',  ( 0.000000000000000000, 0.000000000000000000, 1.000000000000000000 ) ) ;
#8071=ORIENTED_EDGE ( 'NONE', *, *, #14086, .F. ) ;
#8072=VERTEX_POINT ( 'NONE', #8851 ) ;
#8109=DIRECTION ( 'NONE',  ( 0.000000000000000000, 0.000000000000000000, 1.000000000000000000 ) ) ;
#8162=DIRECTION ( 'NONE',  ( 0.000000000000000000, 0.000000000000000000, 1.000000000000000000 ) ) ;
#8170=ORIENTED_EDGE ( 'NONE', *, *, #8404, .T. ) ;
#8176=ORIENTED_EDGE ( 'NONE', *, *, #6869, .T. ) ;
#8249=ORIENTED_EDGE ( 'NONE', *, *, #3905, .T. ) ;
#8250=VECTOR ( 'NONE', #15261, 1000.000000000000000 ) ;
#8258=CARTESIAN_POINT ( 'NONE',  ( 57.41329019055577021, 2.488961461112888074, 127.7236236191910734 ) ) ;
#8267=PRESENTATION_STYLE_ASSIGNMENT (( #3765 ) ) ;
#8284=ORIENTED_EDGE ( 'NONE', *, *, #3763, .F. ) ;
#8285=EDGE_CURVE ( 'NONE', #7936, #9953, #1076, .T. ) ;
#8293=DIRECTION ( 'NONE',  ( -0.000000000000000000, 1.000000000000000000, -0.000000000000000000 ) ) ;
#8337=ORIENTED_EDGE ( 'NONE', *, *, #14754, .F. ) ;
#8358=FACE_OUTER_BOUND ( 'NONE', #8533, .T. ) ;
#8374=PLANE ( 'NONE',  #7798 ) ;
#8404=EDGE_CURVE ( 'NONE', #11245, #8072, #5832, .T. ) ;
#8437=EDGE_LOOP ( 'NONE', ( #9081, #3779, #1527, #5283 ) ) ;
#8490=EDGE_CURVE ( 'NONE', #8984, #3399, #7663, .T. ) ;
#8513=DIRECTION ( 'NONE',  ( 0.000000000000000000, 1.000000000000000000, 0.000000000000000000 ) ) ;
#8515=VERTEX_POINT ( 'NONE', #9194 ) ;
#8533=EDGE_LOOP ( 'NONE', ( #2142, #11098, #10979, #3690 ) ) ;
#8560=MECHANICAL_DESIGN_GEOMETRIC_PRESENTATION_REPRESENTATION('',(#374),#9041);
#8570=ADVANCED_FACE ( 'NONE', ( #10287 ), #4421, .F. ) ;
#8573=SURFACE_SIDE_STYLE ('',( #11759 ) ) ;
#8575=EDGE_LOOP ( 'NONE', ( #10923, #10571, #9661, #10815 ) ) ;
#8580=CARTESIAN_POINT ( 'NONE',  ( -35.58670980944424400, 5.000000000000001776, 93.54081111919107627 ) ) ;
#8593=EDGE_CURVE ( 'NONE', #7307, #9134, #11365, .T. ) ;
#8640=DIRECTION ( 'NONE',  ( -0.000000000000000000, 1.000000000000000000, -0.000000000000000000 ) ) ;
#8641=EDGE_CURVE ( 'NONE', #6629, #15063, #5503, .T. ) ;
#8691=CARTESIAN_POINT ( 'NONE',  ( 0.000000000000000000, 0.000000000000000000, 0.000000000000000000 ) ) ;
#8706=DIRECTION ( 'NONE',  ( 0.000000000000000000, 0.000000000000000000, 1.000000000000000000 ) ) ;
#8733=CARTESIAN_POINT ( 'NONE',  ( -35.58670980944424400, 5.000000000000000000, 97.50956111919106206 ) ) ;
#8765=CONICAL_SURFACE ( 'NONE', #9182, 3.968749999999992895, 0.7155849933176756661 ) ;
#8820=VERTEX_POINT ( 'NONE', #10990 ) ;
#8824=AXIS2_PLACEMENT_3D ( 'NONE', #14116, #7852, #6694 ) ;
#8828=LINE ( 'NONE', #11155, #180 ) ;
#8842=ORIENTED_EDGE ( 'NONE', *, *, #3905, .F. ) ;
#8843=ORIENTED_EDGE ( 'NONE', *, *, #3425, .T. ) ;
#8851=CARTESIAN_POINT ( 'NONE',  ( -46.58670980944423690, 0.000000000000000000, 135.5095611191910621 ) ) ;
#8863=UNCERTAINTY_MEASURE_WITH_UNIT (LENGTH_MEASURE( 1.000000000000000082E-05 ), #4863, 'distance_accuracy_value', 'NONE');
#8894=CARTESIAN_POINT ( 'NONE',  ( -35.58670980944424400, 5.000000000000000000, 99.29549861919106490 ) ) ;
#8946=DIRECTION ( 'NONE',  ( 0.000000000000000000, 0.000000000000000000, 1.000000000000000000 ) ) ;
#8978=CARTESIAN_POINT ( 'NONE',  ( 57.41329019055577021, 2.488961461112888074, 129.5095611191910621 ) ) ;
#8984=VERTEX_POINT ( 'NONE', #12615 ) ;
#9000=CARTESIAN_POINT ( 'NONE',  ( 57.41329019055577021, 5.000000000000000000, 97.50956111919106206 ) ) ;
#9026=ORIENTED_EDGE ( 'NONE', *, *, #11431, .F. ) ;
#9041=( GEOMETRIC_REPRESENTATION_CONTEXT ( 3 ) GLOBAL_UNCERTAINTY_ASSIGNED_CONTEXT ( ( #8863 ) ) GLOBAL_UNIT_ASSIGNED_CONTEXT ( ( #4863, #9496, #13094 ) ) REPRESENTATION_CONTEXT ( 'NONE', 'WORKASPACE' ) );
#9047=VECTOR ( 'NONE', #4814, 1000.000000000000000 ) ;
#9048=ADVANCED_BREP_SHAPE_REPRESENTATION ( '', ( #385, #285 ), #1033 ) ;
#9055=CIRCLE ( 'NONE', #871, 1.785937500000001066 ) ;
#9081=ORIENTED_EDGE ( 'NONE', *, *, #2483, .F. ) ;
#9134=VERTEX_POINT ( 'NONE', #8258 ) ;
#9140=EDGE_CURVE ( 'NONE', #15255, #7295, #4808, .T. ) ;
#9182=AXIS2_PLACEMENT_3D ( 'NONE', #4855, #2511, #14148 ) ;
#9194=CARTESIAN_POINT ( 'NONE',  ( 66.41329019055578442, 0.000000000000000000, 137.5095611191910621 ) ) ;
#9226=ADVANCED_FACE ( 'NONE', ( #13157 ), #8765, .F. ) ;
#9274=DIRECTION ( 'NONE',  ( 0.000000000000000000, 0.000000000000000000, -1.000000000000000000 ) ) ;
#9284=CIRCLE ( 'NONE', #13512, 1.785937500000001066 ) ;
#9291=EDGE_LOOP ( 'NONE', ( #6347, #9325, #6057, #10791 ) ) ;
#9301=LINE ( 'NONE', #1000, #14236 ) ;
#9305=DIRECTION ( 'NONE',  ( 0.000000000000000000, 0.000000000000000000, -1.000000000000000000 ) ) ;
#9307=DIRECTION ( 'NONE',  ( 0.000000000000000000, 0.000000000000000000, 1.000000000000000000 ) ) ;
#9325=ORIENTED_EDGE ( 'NONE', *, *, #4599, .F. ) ;
#9351=ORIENTED_EDGE ( 'NONE', *, *, #13188, .T. ) ;
#9371=DIRECTION ( 'NONE',  ( 0.000000000000000000, -1.000000000000000000, 0.000000000000000000 ) ) ;
#9372=AXIS2_PLACEMENT_3D ( 'NONE', #5271, #14637, #9985 ) ;
#9376=CARTESIAN_POINT ( 'NONE',  ( 22.46142565487374299, 5.000000000000000000, 22.46142565487405918 ) ) ;
#9389=ADVANCED_FACE ( 'NONE', ( #5004 ), #2503, .F. ) ;
#9435=PRODUCT ( 'Part2', 'Part2', '', ( #7267 ) ) ;
#9468=CARTESIAN_POINT ( 'NONE',  ( 57.41329019055577021, 2.488961461112888074, 99.29549861919106490 ) ) ;
#9483=DIRECTION ( 'NONE',  ( 0.000000000000000000, 0.7547095802227716810, 0.6560590289905077199 ) ) ;
#9496=( NAMED_UNIT ( * ) PLANE_ANGLE_UNIT ( ) SI_UNIT ( $, .RADIAN. ) );
#9505=CARTESIAN_POINT ( 'NONE',  ( 57.41329019055577021, 5.000000000000001776, 101.4783111191910621 ) ) ;
#9525=AXIS2_PLACEMENT_3D ( 'NONE', #1103, #6012, #2490 ) ;
#9531=ORIENTED_EDGE ( 'NONE', *, *, #12745, .T. ) ;
#9540=DIRECTION ( 'NONE',  ( 0.000000000000000000, -1.000000000000000000, 0.000000000000000000 ) ) ;
#9562=CARTESIAN_POINT ( 'NONE',  ( -35.58670980944424400, 5.000000000000001776, 101.4783111191910621 ) ) ;
#9584=CYLINDRICAL_SURFACE ( 'NONE', #1889, 1.785937500000001066 ) ;
#9609=EDGE_CURVE ( 'NONE', #14989, #9134, #12457, .T. ) ;
#9644=ORIENTED_EDGE ( 'NONE', *, *, #12120, .F. ) ;
#9654=PLANE ( 'NONE',  #10727 ) ;
#9661=ORIENTED_EDGE ( 'NONE', *, *, #9898, .T. ) ;
#9662=CARTESIAN_POINT ( 'NONE',  ( -35.58670980944424400, 0.000000000000000000, 129.5095611191910621 ) ) ;
#9668=DIRECTION ( 'NONE',  ( 0.7071067811865475727, 0.000000000000000000, -0.7071067811865475727 ) ) ;
#9720=DIRECTION ( 'NONE',  ( 0.000000000000000000, 0.000000000000000000, 1.000000000000000000 ) ) ;
#9736=CARTESIAN_POINT ( 'NONE',  ( -35.58670980944424400, 2.488961461112888074, 99.29549861919106490 ) ) ;
#9750=AXIS2_PLACEMENT_3D ( 'NONE', #6861, #3588, #11581 ) ;
#9762=ORIENTED_EDGE ( 'NONE', *, *, #4338, .T. ) ;
#9834=LINE ( 'NONE', #1465, #11666 ) ;
#9836=CARTESIAN_POINT ( 'NONE',  ( -35.58670980944424400, 2.488961461112888074, 127.7236236191910734 ) ) ;
#9873=AXIS2_PLACEMENT_3D ( 'NONE', #8978, #12781, #6896 ) ;
#9877=ORIENTED_EDGE ( 'NONE', *, *, #11709, .T. ) ;
#9880=ADVANCED_FACE ( 'NONE', ( #12997 ), #6009, .F. ) ;
#9888=DIRECTION ( 'NONE',  ( -0.000000000000000000, 1.000000000000000000, -0.000000000000000000 ) ) ;
#9898=EDGE_CURVE ( 'NONE', #3399, #4506, #4768, .T. ) ;
#9938=UNCERTAINTY_MEASURE_WITH_UNIT (LENGTH_MEASURE( 1.000000000000000082E-05 ), #4952, 'distance_accuracy_value', 'NONE');
#9943=CARTESIAN_POINT ( 'NONE',  ( 66.41329019055577021, 5.000000000000000000, 89.50956111919107627 ) ) ;
#9944=DIRECTION ( 'NONE',  ( -0.7071067811865451302, -0.000000000000000000, 0.7071067811865500152 ) ) ;
#9947=CARTESIAN_POINT ( 'NONE',  ( -35.58670980944424400, 2.488961461112888074, 97.50956111919106206 ) ) ;
#9949=EDGE_CURVE ( 'NONE', #12943, #12948, #7571, .T. ) ;
#9953=VERTEX_POINT ( 'NONE', #5398 ) ;
#9965=EDGE_CURVE ( 'NONE', #5280, #3825, #11123, .T. ) ;
#9985=DIRECTION ( 'NONE',  ( 0.000000000000000000, 0.000000000000000000, 1.000000000000000000 ) ) ;
#9987=CARTESIAN_POINT ( 'NONE',  ( -44.58670980944422269, 5.000000000000000000, 89.50956111919107627 ) ) ;
#9991=CIRCLE ( 'NONE', #1081, 1.785937500000001066 ) ;
#9999=DIRECTION ( 'NONE',  ( 8.034405899049458729E-17, 0.7547095802227716810, -0.6560590289905077199 ) ) ;
#10007=CARTESIAN_POINT ( 'NONE',  ( 68.41329019055577021, 5.000000000000000000, 137.5095611191910621 ) ) ;
#10059=DIRECTION ( 'NONE',  ( 0.000000000000000000, 0.000000000000000000, 1.000000000000000000 ) ) ;
#10066=AXIS2_PLACEMENT_3D ( 'NONE', #13466, #13316, #4935 ) ;
#10090=EDGE_LOOP ( 'NONE', ( #2289, #6908, #10122, #10831 ) ) ;
#10094=DIRECTION ( 'NONE',  ( -0.000000000000000000, 1.000000000000000000, -0.000000000000000000 ) ) ;
#10122=ORIENTED_EDGE ( 'NONE', *, *, #12106, .F. ) ;
#10147=DIRECTION ( 'NONE',  ( -1.000000000000000000, 0.000000000000000000, 0.000000000000000000 ) ) ;
#10184=EDGE_CURVE ( 'NONE', #3401, #7307, #15203, .T. ) ;
#10188=AXIS2_PLACEMENT_3D ( 'NONE', #14126, #11958, #9540 ) ;
#10194=LINE ( 'NONE', #7594, #14654 ) ;
#10204=CARTESIAN_POINT ( 'NONE',  ( -91.04813546431763882, 5.000000000000000000, 91.04813546431763882 ) ) ;
#10206=LINE ( 'NONE', #3164, #14501 ) ;
#10229=DIRECTION ( 'NONE',  ( 0.000000000000000000, 0.000000000000000000, 1.000000000000000000 ) ) ;
#10243=AXIS2_PLACEMENT_3D ( 'NONE', #1457, #129, #13025 ) ;
#10265=CARTESIAN_POINT ( 'NONE',  ( 57.41329019055577021, 5.000000000000001776, 133.4783111191910621 ) ) ;
#10287=FACE_OUTER_BOUND ( 'NONE', #7034, .T. ) ;
#10327=LINE ( 'NONE', #12892, #1292 ) ;
#10338=LINE ( 'NONE', #7939, #3755 ) ;
#10346=VECTOR ( 'NONE', #13042, 1000.000000000000114 ) ;
#10347=DIRECTION ( 'NONE',  ( 0.000000000000000000, 0.7547095802227716810, 0.6560590289905077199 ) ) ;
#10359=ADVANCED_FACE ( 'NONE', ( #3498 ), #7233, .F. ) ;
#10372=ORIENTED_EDGE ( 'NONE', *, *, #912, .F. ) ;
#10419=CARTESIAN_POINT ( 'NONE',  ( -35.58670980944424400, 2.488961461112888074, 129.5095611191910621 ) ) ;
#10473=EDGE_CURVE ( 'NONE', #10769, #8820, #12189, .T. ) ;
#10513=DIRECTION ( 'NONE',  ( 0.000000000000000000, -1.000000000000000000, 0.000000000000000000 ) ) ;
#10542=FACE_OUTER_BOUND ( 'NONE', #8575, .T. ) ;
#10571=ORIENTED_EDGE ( 'NONE', *, *, #13526, .F. ) ;
#10586=DIRECTION ( 'NONE',  ( -0.000000000000000000, 1.000000000000000000, -0.000000000000000000 ) ) ;
#10590=ORIENTED_EDGE ( 'NONE', *, *, #14365, .F. ) ;
#10659=EDGE_CURVE ( 'NONE', #6026, #5280, #4026, .T. ) ;
#10668=ADVANCED_FACE ( 'NONE', ( #4641 ), #5664, .F. ) ;
#10673=CARTESIAN_POINT ( 'NONE',  ( -35.58670980944424400, 0.000000000000000000, 97.50956111919106206 ) ) ;
#10679=ORIENTED_EDGE ( 'NONE', *, *, #1489, .F. ) ;
#10688=CARTESIAN_POINT ( 'NONE',  ( -46.58670980944423690, 0.000000000000000000, 91.50956111919106206 ) ) ;
#10696=DIRECTION ( 'NONE',  ( -0.7071067811865525687, -0.000000000000000000, 0.7071067811865425767 ) ) ;
#10727=AXIS2_PLACEMENT_3D ( 'NONE', #2609, #1290, #11848 ) ;
#10740=EDGE_LOOP ( 'NONE', ( #12396, #11609, #8337, #1338 ) ) ;
#10742=VECTOR ( 'NONE', #12983, 1000.000000000000000 ) ;
#10769=VERTEX_POINT ( 'NONE', #9505 ) ;
#10770=ADVANCED_FACE ( 'NONE', ( #2690, #4946, #3699, #7129, #7204 ), #9654, .T. ) ;
#10791=ORIENTED_EDGE ( 'NONE', *, *, #13526, .T. ) ;
#10806=CARTESIAN_POINT ( 'NONE',  ( 57.41329019055577021, 5.000000000000001776, 129.5095611191910621 ) ) ;
#10815=ORIENTED_EDGE ( 'NONE', *, *, #13810, .T. ) ;
#10818=VECTOR ( 'NONE', #7715, 1000.000000000000000 ) ;
#10831=ORIENTED_EDGE ( 'NONE', *, *, #9949, .F. ) ;
#10902=ORIENTED_EDGE ( 'NONE', *, *, #4198, .T. ) ;
#10916=PLANE ( 'NONE',  #10243 ) ;
#10919=ORIENTED_EDGE ( 'NONE', *, *, #1435, .F. ) ;
#10923=ORIENTED_EDGE ( 'NONE', *, *, #5753, .F. ) ;
#10961=EDGE_LOOP ( 'NONE', ( #5497, #8176, #15252, #2895 ) ) ;
#10979=ORIENTED_EDGE ( 'NONE', *, *, #1489, .T. ) ;
#10990=CARTESIAN_POINT ( 'NONE',  ( 57.41329019055577021, 5.000000000000001776, 93.54081111919107627 ) ) ;
#11001=EDGE_LOOP ( 'NONE', ( #11624, #13761, #1276, #9531 ) ) ;
#11003=VECTOR ( 'NONE', #338, 1000.000000000000000 ) ;
#11042=EDGE_CURVE ( 'NONE', #9953, #1111, #4753, .T. ) ;
#11053=CIRCLE ( 'NONE', #14982, 1.785937500000001066 ) ;
#11055=CARTESIAN_POINT ( 'NONE',  ( -35.58670980944424400, 5.000000000000001776, 129.5095611191910621 ) ) ;
#11071=AXIS2_PLACEMENT_3D ( 'NONE', #11987, #8640, #6193 ) ;
#11093=ORIENTED_EDGE ( 'NONE', *, *, #13764, .T. ) ;
#11098=ORIENTED_EDGE ( 'NONE', *, *, #7264, .T. ) ;
#11119=CYLINDRICAL_SURFACE ( 'NONE', #529, 1.785937500000001066 ) ;
#11123=LINE ( 'NONE', #7646, #1773 ) ;
#11144=DIRECTION ( 'NONE',  ( 0.7071067811865425767, -0.000000000000000000, 0.7071067811865525687 ) ) ;
#11154=DIRECTION ( 'NONE',  ( 0.000000000000000000, -1.000000000000000000, 0.000000000000000000 ) ) ;
#11155=CARTESIAN_POINT ( 'NONE',  ( 57.41329019055577021, 5.000000000000001776, 93.54081111919107627 ) ) ;
#11168=CARTESIAN_POINT ( 'NONE',  ( -35.58670980944424400, 5.000000000000001776, 125.5408111191910763 ) ) ;
#11172=DIRECTION ( 'NONE',  ( -0.000000000000000000, 1.000000000000000000, -0.000000000000000000 ) ) ;
#11194=DIRECTION ( 'NONE',  ( 0.000000000000000000, 1.000000000000000000, 0.000000000000000000 ) ) ;
#11220=ORIENTED_EDGE ( 'NONE', *, *, #3425, .F. ) ;
#11245=VERTEX_POINT ( 'NONE', #3036 ) ;
#11261=DIRECTION ( 'NONE',  ( 0.000000000000000000, 1.000000000000000000, 0.000000000000000000 ) ) ;
#11271=CONICAL_SURFACE ( 'NONE', #6331, 3.968749999999992895, 0.7155849933176756661 ) ;
#11287=COLOUR_RGB ( '', 0.40784314, 0.44705882, 0.49803922) ;
#11289=CARTESIAN_POINT ( 'NONE',  ( 57.41329019055577021, 5.000000000000000000, 127.7236236191910734 ) ) ;
#11313=EDGE_LOOP ( 'NONE', ( #3656, #1593, #6652, #10919 ) ) ;
#11335=DIRECTION ( 'NONE',  ( 0.000000000000000000, 0.000000000000000000, 1.000000000000000000 ) ) ;
#11365=CIRCLE ( 'NONE', #9873, 1.785937500000001066 ) ;
#11378=DIRECTION ( 'NONE',  ( -0.000000000000000000, 1.000000000000000000, -0.000000000000000000 ) ) ;
#11391=ORIENTED_EDGE ( 'NONE', *, *, #4513, .T. ) ;
#11403=CARTESIAN_POINT ( 'NONE',  ( 57.41329019055577021, 2.488961461112888074, 97.50956111919106206 ) ) ;
#11431=EDGE_CURVE ( 'NONE', #6301, #6290, #3414, .T. ) ;
#11462=DIRECTION ( 'NONE',  ( -0.000000000000000000, 1.000000000000000000, -0.000000000000000000 ) ) ;
#11495=CIRCLE ( 'NONE', #5056, 1.785937500000001066 ) ;
#11506=CLOSED_SHELL ( 'NONE', ( #3527, #15024, #8570, #1592, #13236, #4817, #9226, #2278, #14634, #13484, #6807, #2893, #10770, #12583, #7086, #9389, #4869, #904, #10668, #9880, #711, #3522, #14277, #3262, #10359, #14167 ) ) ;
#11572=EDGE_LOOP ( 'NONE', ( #8284, #7708, #8249, #5482 ) ) ;
#11581=DIRECTION ( 'NONE',  ( 0.000000000000000000, 0.000000000000000000, 1.000000000000000000 ) ) ;
#11609=ORIENTED_EDGE ( 'NONE', *, *, #4221, .T. ) ;
#11615=CARTESIAN_POINT ( 'NONE',  ( -46.58670980944423690, 5.000000000000000000, 91.50956111919106206 ) ) ;
#11624=ORIENTED_EDGE ( 'NONE', *, *, #6325, .F. ) ;
#11642=ORIENTED_EDGE ( 'NONE', *, *, #11709, .F. ) ;
#11666=VECTOR ( 'NONE', #11154, 1000.000000000000000 ) ;
#11704=FACE_OUTER_BOUND ( 'NONE', #11313, .T. ) ;
#11709=EDGE_CURVE ( 'NONE', #188, #7936, #6449, .T. ) ;
#11725=VECTOR ( 'NONE', #2424, 1000.000000000000000 ) ;
#11754=CARTESIAN_POINT ( 'NONE',  ( 57.41329019055577021, 5.000000000000001776, 129.5095611191910621 ) ) ;
#11759=SURFACE_STYLE_FILL_AREA ( #14463 ) ;
#11765=PLANE ( 'NONE',  #5232 ) ;
#11775=ORIENTED_EDGE ( 'NONE', *, *, #1470, .F. ) ;
#11784=LINE ( 'NONE', #10688, #6330 ) ;
#11785=AXIS2_PLACEMENT_3D ( 'NONE', #13540, #14601, #2905 ) ;
#11801=VECTOR ( 'NONE', #8162, 1000.000000000000000 ) ;
#11848=DIRECTION ( 'NONE',  ( 0.000000000000000000, -0.000000000000000000, 1.000000000000000000 ) ) ;
#11854=( NAMED_UNIT ( * ) PLANE_ANGLE_UNIT ( ) SI_UNIT ( $, .RADIAN. ) );
#11869=DIRECTION ( 'NONE',  ( 0.000000000000000000, 0.000000000000000000, 1.000000000000000000 ) ) ;
#11874=ORIENTED_EDGE ( 'NONE', *, *, #10473, .T. ) ;
#11902=DIRECTION ( 'NONE',  ( 0.000000000000000000, 0.000000000000000000, 1.000000000000000000 ) ) ;
#11922=CARTESIAN_POINT ( 'NONE',  ( 57.41329019055577021, 0.000000000000000000, 131.2954986191910791 ) ) ;
#11938=FACE_OUTER_BOUND ( 'NONE', #4253, .T. ) ;
#11958=DIRECTION ( 'NONE',  ( -0.7071067811865524577, 0.000000000000000000, 0.7071067811865425767 ) ) ;
#11987=CARTESIAN_POINT ( 'NONE',  ( 57.41329019055577021, 5.000000000000001776, 97.50956111919106206 ) ) ;
#12007=FACE_OUTER_BOUND ( 'NONE', #9291, .T. ) ;
#12023=DIRECTION ( 'NONE',  ( 0.000000000000000000, -1.000000000000000000, 0.000000000000000000 ) ) ;
#12056=EDGE_LOOP ( 'NONE', ( #15173, #131, #12514, #7904 ) ) ;
#12093=DIRECTION ( 'NONE',  ( 0.000000000000000000, 0.000000000000000000, 1.000000000000000000 ) ) ;
#12106=EDGE_CURVE ( 'NONE', #12948, #6290, #10194, .T. ) ;
#12109=ORIENTED_EDGE ( 'NONE', *, *, #4472, .T. ) ;
#12120=EDGE_CURVE ( 'NONE', #3694, #3399, #13707, .T. ) ;
#12151=LINE ( 'NONE', #441, #2089 ) ;
#12159=ORIENTED_EDGE ( 'NONE', *, *, #13188, .F. ) ;
#12164=AXIS2_PLACEMENT_3D ( 'NONE', #11055, #498, #9720 ) ;
#12189=CIRCLE ( 'NONE', #1536, 3.968749999999992895 ) ;
#12192=DIRECTION ( 'NONE',  ( 0.000000000000000000, 0.000000000000000000, 1.000000000000000000 ) ) ;
#12226=VECTOR ( 'NONE', #10347, 1000.000000000000000 ) ;
#12333=LINE ( 'NONE', #4966, #6112 ) ;
#12371=CARTESIAN_POINT ( 'NONE',  ( 68.41329019055577021, 0.000000000000000000, 91.50956111919110469 ) ) ;
#12374=DIRECTION ( 'NONE',  ( 0.000000000000000000, 0.000000000000000000, -1.000000000000000000 ) ) ;
#12396=ORIENTED_EDGE ( 'NONE', *, *, #11431, .T. ) ;
#12409=VERTEX_POINT ( 'NONE', #13161 ) ;
#12415=ORIENTED_EDGE ( 'NONE', *, *, #3763, .T. ) ;
#12425=CYLINDRICAL_SURFACE ( 'NONE', #1896, 1.785937500000001066 ) ;
#12455=AXIS2_PLACEMENT_3D ( 'NONE', #8691, #1325, #2650 ) ;
#12457=LINE ( 'NONE', #11289, #14143 ) ;
#12494=EDGE_CURVE ( 'NONE', #3825, #10769, #10327, .T. ) ;
#12514=ORIENTED_EDGE ( 'NONE', *, *, #2483, .T. ) ;
#12516=ORIENTED_EDGE ( 'NONE', *, *, #4599, .T. ) ;
#12573=ORIENTED_EDGE ( 'NONE', *, *, #6869, .F. ) ;
#12583=ADVANCED_FACE ( 'NONE', ( #6007, #3892, #5057, #13206, #4913 ), #6314, .F. ) ;
#12598=LINE ( 'NONE', #14976, #10818 ) ;
#12615=CARTESIAN_POINT ( 'NONE',  ( -35.58670980944424400, 2.488961461112888074, 95.72362361919107343 ) ) ;
#12618=DIRECTION ( 'NONE',  ( -0.000000000000000000, 1.000000000000000000, -0.000000000000000000 ) ) ;
#12628=DIRECTION ( 'NONE',  ( 0.000000000000000000, 1.000000000000000000, 0.000000000000000000 ) ) ;
#12633=ORIENTED_EDGE ( 'NONE', *, *, #6506, .T. ) ;
#12635=ORIENTED_EDGE ( 'NONE', *, *, #14754, .T. ) ;
#12668=VERTEX_POINT ( 'NONE', #3029 ) ;
#12718=EDGE_CURVE ( 'NONE', #14870, #12409, #4197, .T. ) ;
#12745=EDGE_CURVE ( 'NONE', #8515, #6954, #5521, .T. ) ;
#12749=VECTOR ( 'NONE', #12628, 1000.000000000000000 ) ;
#12763=AXIS2_PLACEMENT_3D ( 'NONE', #1716, #14511, #12192 ) ;
#12777=CARTESIAN_POINT ( 'NONE',  ( 57.41329019055577021, 2.488961461112888074, 97.50956111919106206 ) ) ;
#12781=DIRECTION ( 'NONE',  ( -0.000000000000000000, 1.000000000000000000, -0.000000000000000000 ) ) ;
#12782=DIRECTION ( 'NONE',  ( 0.000000000000000000, 0.000000000000000000, 1.000000000000000000 ) ) ;
#12802=CIRCLE ( 'NONE', #11071, 3.968749999999992895 ) ;
#12812=EDGE_CURVE ( 'NONE', #467, #2967, #1784, .T. ) ;
#12856=CARTESIAN_POINT ( 'NONE',  ( -46.58670980944423690, 5.000000000000000000, 89.50956111919107627 ) ) ;
#12866=CARTESIAN_POINT ( 'NONE',  ( 57.41329019055577021, 2.488961461112888074, 95.72362361919107343 ) ) ;
#12882=DIRECTION ( 'NONE',  ( 0.000000000000000000, 1.000000000000000000, 0.000000000000000000 ) ) ;
#12892=CARTESIAN_POINT ( 'NONE',  ( 57.41329019055577021, 5.000000000000001776, 101.4783111191910621 ) ) ;
#12940=EDGE_CURVE ( 'NONE', #1111, #8072, #6758, .T. ) ;
#12943=VERTEX_POINT ( 'NONE', #4657 ) ;
#12948=VERTEX_POINT ( 'NONE', #2317 ) ;
#12978=AXIS2_PLACEMENT_3D ( 'NONE', #7650, #12374, #2825 ) ;
#12983=DIRECTION ( 'NONE',  ( -1.000000000000000000, -0.000000000000000000, -0.000000000000000000 ) ) ;
#12987=EDGE_LOOP ( 'NONE', ( #12109, #211 ) ) ;
#12992=AXIS2_PLACEMENT_3D ( 'NONE', #6481, #11194, #14764 ) ;
#12997=FACE_OUTER_BOUND ( 'NONE', #1652, .T. ) ;
#13025=DIRECTION ( 'NONE',  ( 1.000000000000000000, 0.000000000000000000, -0.000000000000000000 ) ) ;
#13042=DIRECTION ( 'NONE',  ( -0.7071067811865474617, 0.000000000000000000, -0.7071067811865474617 ) ) ;
#13043=CARTESIAN_POINT ( 'NONE',  ( 57.41329019055577021, 5.000000000000001776, 97.50956111919106206 ) ) ;
#13060=PRODUCT_DEFINITION_SHAPE ( 'NONE', 'NONE',  #13774 ) ;
#13094=( NAMED_UNIT ( * ) SI_UNIT ( $, .STERADIAN. ) SOLID_ANGLE_UNIT ( ) );
#13099=DIRECTION ( 'NONE',  ( 1.000000000000000000, 0.000000000000000000, 0.000000000000000000 ) ) ;
#13157=FACE_OUTER_BOUND ( 'NONE', #8437, .T. ) ;
#13161=CARTESIAN_POINT ( 'NONE',  ( -35.58670980944424400, 2.488961461112888074, 131.2954986191910791 ) ) ;
#13188=EDGE_CURVE ( 'NONE', #7307, #7295, #6802, .T. ) ;
#13206=FACE_BOUND ( 'NONE', #4889, .T. ) ;
#13212=VECTOR ( 'NONE', #11172, 1000.000000000000000 ) ;
#13230=CARTESIAN_POINT ( 'NONE',  ( -35.58670980944424400, 5.000000000000000000, 95.72362361919107343 ) ) ;
#13234=CIRCLE ( 'NONE', #9750, 3.968749999999992895 ) ;
#13236=ADVANCED_FACE ( 'NONE', ( #7730 ), #14203, .F. ) ;
#13237=EDGE_CURVE ( 'NONE', #1968, #12943, #15073, .T. ) ;
#13282=VECTOR ( 'NONE', #7843, 1000.000000000000000 ) ;
#13292=CARTESIAN_POINT ( 'NONE',  ( -35.58670980944424400, 0.000000000000000000, 129.5095611191910621 ) ) ;
#13316=DIRECTION ( 'NONE',  ( -0.000000000000000000, 1.000000000000000000, -0.000000000000000000 ) ) ;
#13318=AXIS2_PLACEMENT_3D ( 'NONE', #10007, #10147, #7847 ) ;
#13332=CARTESIAN_POINT ( 'NONE',  ( -35.58670980944424400, 5.000000000000000000, 97.50956111919106206 ) ) ;
#13405=ORIENTED_EDGE ( 'NONE', *, *, #13677, .T. ) ;
#13411=EDGE_LOOP ( 'NONE', ( #13405, #12415 ) ) ;
#13462=DIRECTION ( 'NONE',  ( -0.000000000000000000, 1.000000000000000000, -0.000000000000000000 ) ) ;
#13466=CARTESIAN_POINT ( 'NONE',  ( -35.58670980944424400, 5.000000000000001776, 129.5095611191910621 ) ) ;
#13484=ADVANCED_FACE ( 'NONE', ( #185 ), #7337, .F. ) ;
#13498=VECTOR ( 'NONE', #9999, 1000.000000000000000 ) ;
#13512=AXIS2_PLACEMENT_3D ( 'NONE', #13292, #3333, #14881 ) ;
#13514=DIRECTION ( 'NONE',  ( 0.000000000000000000, 1.000000000000000000, 0.000000000000000000 ) ) ;
#13526=EDGE_CURVE ( 'NONE', #3399, #8984, #11495, .T. ) ;
#13540=CARTESIAN_POINT ( 'NONE',  ( -35.58670980944424400, 5.000000000000001776, 97.50956111919106206 ) ) ;
#13550=EDGE_CURVE ( 'NONE', #7940, #8984, #3756, .T. ) ;
#13581=CARTESIAN_POINT ( 'NONE',  ( -35.58670980944424400, 2.488961461112888074, 129.5095611191910621 ) ) ;
#13605=CARTESIAN_POINT ( 'NONE',  ( 57.41329019055577021, 5.000000000000000000, 97.50956111919106206 ) ) ;
#13610=LINE ( 'NONE', #2978, #13770 ) ;
#13637=ORIENTED_EDGE ( 'NONE', *, *, #4021, .F. ) ;
#13660=LINE ( 'NONE', #765, #2148 ) ;
#13677=EDGE_CURVE ( 'NONE', #3401, #14989, #4549, .T. ) ;
#13707=LINE ( 'NONE', #8894, #3025 ) ;
#13732=ORIENTED_EDGE ( 'NONE', *, *, #1470, .T. ) ;
#13748=ORIENTED_EDGE ( 'NONE', *, *, #10473, .F. ) ;
#13755=CARTESIAN_POINT ( 'NONE',  ( 57.41329019055577021, 5.000000000000000000, 131.2954986191910791 ) ) ;
#13761=ORIENTED_EDGE ( 'NONE', *, *, #1435, .T. ) ;
#13763=CARTESIAN_POINT ( 'NONE',  ( 57.41329019055577021, 5.000000000000000000, 129.5095611191910621 ) ) ;
#13764=EDGE_CURVE ( 'NONE', #12943, #7936, #4521, .T. ) ;
#13770=VECTOR ( 'NONE', #9944, 1000.000000000000114 ) ;
#13774=PRODUCT_DEFINITION ( 'UNKNOWN', '', #6453, #4060 ) ;
#13788=ORIENTED_EDGE ( 'NONE', *, *, #9898, .F. ) ;
#13810=EDGE_CURVE ( 'NONE', #4506, #12668, #13234, .T. ) ;
#13865=CARTESIAN_POINT ( 'NONE',  ( 57.41329019055577021, 0.000000000000000000, 97.50956111919106206 ) ) ;
#13890=ORIENTED_EDGE ( 'NONE', *, *, #1366, .T. ) ;
#14017=DIRECTION ( 'NONE',  ( -0.000000000000000000, 1.000000000000000000, -0.000000000000000000 ) ) ;
#14023=CARTESIAN_POINT ( 'NONE',  ( -35.58670980944424400, 5.000000000000001776, 125.5408111191910763 ) ) ;
#14086=EDGE_CURVE ( 'NONE', #2967, #2765, #1707, .T. ) ;
#14116=CARTESIAN_POINT ( 'NONE',  ( -35.58670980944424400, 5.000000000000001776, 97.50956111919106206 ) ) ;
#14126=CARTESIAN_POINT ( 'NONE',  ( 66.41329019055577021, 5.000000000000000000, 89.50956111919107627 ) ) ;
#14143=VECTOR ( 'NONE', #732, 1000.000000000000000 ) ;
#14148=DIRECTION ( 'NONE',  ( 0.000000000000000000, 0.000000000000000000, 1.000000000000000000 ) ) ;
#14167=ADVANCED_FACE ( 'NONE', ( #3558 ), #6065, .F. ) ;
#14203=CONICAL_SURFACE ( 'NONE', #7030, 3.968749999999992895, 0.7155849933176756661 ) ;
#14236=VECTOR ( 'NONE', #12882, 1000.000000000000000 ) ;
#14238=FACE_OUTER_BOUND ( 'NONE', #4010, .T. ) ;
#14241=FACE_OUTER_BOUND ( 'NONE', #5051, .T. ) ;
#14259=CARTESIAN_POINT ( 'NONE',  ( 68.41329019055577021, 5.000000000000000000, 135.5095611191910621 ) ) ;
#14266=EDGE_CURVE ( 'NONE', #1111, #188, #11784, .T. ) ;
#14277=ADVANCED_FACE ( 'NONE', ( #11704 ), #8374, .F. ) ;
#14319=CARTESIAN_POINT ( 'NONE',  ( 57.41329019055577021, 5.000000000000001776, 97.50956111919106206 ) ) ;
#14327=( NAMED_UNIT ( * ) SI_UNIT ( $, .STERADIAN. ) SOLID_ANGLE_UNIT ( ) );
#14339=LINE ( 'NONE', #2401, #9047 ) ;
#14365=EDGE_CURVE ( 'NONE', #14499, #6301, #9834, .T. ) ;
#14382=ORIENTED_EDGE ( 'NONE', *, *, #5565, .F. ) ;
#14408=DIRECTION ( 'NONE',  ( 0.000000000000000000, 0.7547095802227716810, 0.6560590289905077199 ) ) ;
#14444=CARTESIAN_POINT ( 'NONE',  ( -35.58670980944424400, 5.000000000000001776, 133.4783111191910621 ) ) ;
#14452=VECTOR ( 'NONE', #9305, 1000.000000000000000 ) ;
#14463=FILL_AREA_STYLE ('',( #261 ) ) ;
#14477=ORIENTED_EDGE ( 'NONE', *, *, #6325, .T. ) ;
#14499=VERTEX_POINT ( 'NONE', #15084 ) ;
#14501=VECTOR ( 'NONE', #3231, 1000.000000000000000 ) ;
#14511=DIRECTION ( 'NONE',  ( -0.000000000000000000, 1.000000000000000000, -0.000000000000000000 ) ) ;
#14515=EDGE_LOOP ( 'NONE', ( #723, #5384, #6771, #9644 ) ) ;
#14530=DIRECTION ( 'NONE',  ( 0.000000000000000000, 0.000000000000000000, 1.000000000000000000 ) ) ;
#14540=ORIENTED_EDGE ( 'NONE', *, *, #8593, .T. ) ;
#14601=DIRECTION ( 'NONE',  ( -0.000000000000000000, 1.000000000000000000, -0.000000000000000000 ) ) ;
#14634=ADVANCED_FACE ( 'NONE', ( #14238 ), #11765, .F. ) ;
#14637=DIRECTION ( 'NONE',  ( -0.000000000000000000, 1.000000000000000000, -0.000000000000000000 ) ) ;
#14654=VECTOR ( 'NONE', #11144, 999.9999999999998863 ) ;
#14677=DIRECTION ( 'NONE',  ( -0.000000000000000000, 1.000000000000000000, -0.000000000000000000 ) ) ;
#14742=DIRECTION ( 'NONE',  ( 0.000000000000000000, 0.000000000000000000, 1.000000000000000000 ) ) ;
#14747=CARTESIAN_POINT ( 'NONE',  ( 68.41329019055577021, 5.000000000000000000, 91.50956111919110469 ) ) ;
#14754=EDGE_CURVE ( 'NONE', #14499, #1968, #10338, .T. ) ;
#14764=DIRECTION ( 'NONE',  ( 0.000000000000000000, 0.000000000000000000, 1.000000000000000000 ) ) ;
#14769=CIRCLE ( 'NONE', #4624, 1.785937500000001066 ) ;
#14770=ORIENTED_EDGE ( 'NONE', *, *, #119, .T. ) ;
#14818=ORIENTED_EDGE ( 'NONE', *, *, #15018, .F. ) ;
#14870=VERTEX_POINT ( 'NONE', #2578 ) ;
#14881=DIRECTION ( 'NONE',  ( 0.000000000000000000, 0.000000000000000000, 1.000000000000000000 ) ) ;
#14882=FACE_OUTER_BOUND ( 'NONE', #3360, .T. ) ;
#14932=VERTEX_POINT ( 'NONE', #14444 ) ;
#14934=VECTOR ( 'NONE', #3216, 999.9999999999998863 ) ;
#14936=CARTESIAN_POINT ( 'NONE',  ( 57.41329019055577021, 5.000000000000001776, 133.4783111191910621 ) ) ;
#14939=DIRECTION ( 'NONE',  ( 0.7071067811865474617, -0.000000000000000000, 0.7071067811865474617 ) ) ;
#14972=CIRCLE ( 'NONE', #9525, 1.785937500000001066 ) ;
#14976=CARTESIAN_POINT ( 'NONE',  ( -46.58670980944423690, 5.000000000000000000, 137.5095611191910621 ) ) ;
#14982=AXIS2_PLACEMENT_3D ( 'NONE', #10673, #2151, #5812 ) ;
#14985=ORIENTED_EDGE ( 'NONE', *, *, #9140, .T. ) ;
#14989=VERTEX_POINT ( 'NONE', #5225 ) ;
#14996=CARTESIAN_POINT ( 'NONE',  ( -35.58670980944424400, 5.000000000000001776, 97.50956111919106206 ) ) ;
#15008=CIRCLE ( 'NONE', #15266, 1.785937500000001066 ) ;
#15018=EDGE_CURVE ( 'NONE', #2765, #14932, #4007, .T. ) ;
#15024=ADVANCED_FACE ( 'NONE', ( #414 ), #11119, .F. ) ;
#15049=VECTOR ( 'NONE', #10696, 999.9999999999998863 ) ;
#15054=DIRECTION ( 'NONE',  ( 0.000000000000000000, 0.7547095802227716810, 0.6560590289905077199 ) ) ;
#15059=AXIS2_PLACEMENT_3D ( 'NONE', #4250, #14017, #3229 ) ;
#15063=VERTEX_POINT ( 'NONE', #5159 ) ;
#15073=LINE ( 'NONE', #6875, #14934 ) ;
#15084=CARTESIAN_POINT ( 'NONE',  ( 68.41329019055577021, 5.000000000000000000, 135.5095611191910621 ) ) ;
#15096=ORIENTED_EDGE ( 'NONE', *, *, #12718, .T. ) ;
#15118=ORIENTED_EDGE ( 'NONE', *, *, #4472, .F. ) ;
#15134=EDGE_LOOP ( 'NONE', ( #3552, #7597, #6863, #14540 ) ) ;
#15173=ORIENTED_EDGE ( 'NONE', *, *, #119, .F. ) ;
#15194=CARTESIAN_POINT ( 'NONE',  ( -35.58670980944424400, 5.000000000000000000, 129.5095611191910621 ) ) ;
#15203=LINE ( 'NONE', #13755, #5018 ) ;
#15217=ORIENTED_EDGE ( 'NONE', *, *, #11042, .F. ) ;
#15219=ORIENTED_EDGE ( 'NONE', *, *, #6246, .T. ) ;
#15252=ORIENTED_EDGE ( 'NONE', *, *, #7330, .T. ) ;
#15255=VERTEX_POINT ( 'NONE', #7995 ) ;
#15261=DIRECTION ( 'NONE',  ( 0.000000000000000000, 0.000000000000000000, 1.000000000000000000 ) ) ;
#15263=CARTESIAN_POINT ( 'NONE',  ( 66.41329019055578442, 5.000000000000000000, 137.5095611191910621 ) ) ;
#15266=AXIS2_PLACEMENT_3D ( 'NONE', #10419, #10586, #5885 ) ;
ENDSEC;
END-ISO-10303-21;
